ISO-10303-21;
HEADER;
FILE_DESCRIPTION (('STEP AP214'),
    '1' );
FILE_NAME ('socket head cap screw_iso_ISO 4762 M5 x 30 - 22N.step',
    '2026-10-24T07:08:27',
    ( '' ),
    ( '' ),
    'SwSTEP 2.0',
    'SolidWorks 2026',
    '' );
FILE_SCHEMA (( 'AUTOMOTIVE_DESIGN' ));
ENDSEC;

DATA;
#17=DIRECTION ( 'NONE',  ( 1.000000000000000000, 0.000000000000000000, 0.000000000000000000 ) ) ;
#36=EDGE_LOOP ( 'NONE', ( #215, #7288, #18290, #7153 ) ) ;
#91=VERTEX_POINT ( 'NONE', #6771 ) ;
#105=CLOSED_SHELL ( 'NONE', ( #14234, #17974, #624, #15916, #1588, #4692, #10387, #5528, #1896, #13092, #10492, #15607, #17035, #1733, #4595, #8031, #12836, #9009, #1125, #979, #15240, #9740, #15546, #17077, #15957, #7073, #5906 ) ) ;
#125=VERTEX_POINT ( 'NONE', #12966 ) ;
#186=VERTEX_POINT ( 'NONE', #14473 ) ;
#202=VERTEX_POINT ( 'NONE', #4387 ) ;
#215=ORIENTED_EDGE ( 'NONE', *, *, #7148, .F. ) ;
#224=CARTESIAN_POINT ( 'NONE',  ( 2.500000000000000000, 0.000000000000000000, 0.000000000000000000 ) ) ;
#250=ORIENTED_EDGE ( 'NONE', *, *, #2735, .T. ) ;
#260=EDGE_LOOP ( 'NONE', ( #2275, #5980, #9068 ) ) ;
#337=VECTOR ( 'NONE', #1446, 1000.000000000000114 ) ;
#410=CARTESIAN_POINT ( 'NONE',  ( -31.74999999999995737, 0.000000000000000000, 0.000000000000000000 ) ) ;
#536=FACE_BOUND ( 'NONE', #6514, .T. ) ;
#548=AXIS2_PLACEMENT_3D ( 'NONE', #1931, #7836, #7731 ) ;
#581=CIRCLE ( 'NONE', #11233, 2.500000000000000888 ) ;
#584=CARTESIAN_POINT ( 'NONE',  ( -31.74999999999995737, 5.204748896376250699E-16, -4.250000000000000000 ) ) ;
#603=CARTESIAN_POINT ( 'NONE',  ( 5.000000000000004441, 5.204748896376250699E-16, -4.250000000000000000 ) ) ;
#613=ORIENTED_EDGE ( 'NONE', *, *, #5750, .F. ) ;
#624=ADVANCED_FACE ( 'NONE', ( #11857 ), #1293, .F. ) ;
#634=ORIENTED_EDGE ( 'NONE', *, *, #3408, .F. ) ;
#674=FACE_OUTER_BOUND ( 'NONE', #9063, .T. ) ;
#694=CARTESIAN_POINT ( 'NONE',  ( 0.000000000000000000, -1.178949249685218081, -2.041999999999998039 ) ) ;
#721=DIRECTION ( 'NONE',  ( 1.000000000000000000, 0.000000000000000000, 0.000000000000000000 ) ) ;
#746=EDGE_CURVE ( 'NONE', #9477, #9087, #6433, .T. ) ;
#753=CARTESIAN_POINT ( 'NONE',  ( 2.500000000000000000, -1.178949249685213863, 2.042000000000001148 ) ) ;
#761=ORIENTED_EDGE ( 'NONE', *, *, #2237, .T. ) ;
#773=PRODUCT_DEFINITION_FORMATION_WITH_SPECIFIED_SOURCE ( 'ANY', '', #8595, .NOT_KNOWN. ) ;
#785=EDGE_LOOP ( 'NONE', ( #13312, #6543 ) ) ;
#800=AXIS2_PLACEMENT_3D ( 'NONE', #11341, #18486, #12677 ) ;
#823=CARTESIAN_POINT ( 'NONE',  ( 5.000000000000000888, 4.250000000000000000, 0.000000000000000000 ) ) ;
#847=AXIS2_PLACEMENT_3D ( 'NONE', #1102, #721, #15482 ) ;
#858=VERTEX_POINT ( 'NONE', #12806 ) ;
#865=EDGE_CURVE ( 'NONE', #2263, #4026, #17287, .T. ) ;
#910=CARTESIAN_POINT ( 'NONE',  ( 0.2500000000000002220, 0.000000000000000000, 4.000000000000000000 ) ) ;
#950=ORIENTED_EDGE ( 'NONE', *, *, #13546, .T. ) ;
#979=ADVANCED_FACE ( 'NONE', ( #674 ), #9325, .F. ) ;
#1004=ORIENTED_EDGE ( 'NONE', *, *, #9404, .T. ) ;
#1027=ORIENTED_EDGE ( 'NONE', *, *, #8334, .T. ) ;
#1030=UNCERTAINTY_MEASURE_WITH_UNIT (LENGTH_MEASURE( 1.000000000000000082E-05 ), #12629, 'distance_accuracy_value', 'NONE');
#1040=ORIENTED_EDGE ( 'NONE', *, *, #746, .T. ) ;
#1069=( GEOMETRIC_REPRESENTATION_CONTEXT ( 3 ) GLOBAL_UNCERTAINTY_ASSIGNED_CONTEXT ( ( #5594 ) ) GLOBAL_UNIT_ASSIGNED_CONTEXT ( ( #8899, #15869, #7467 ) ) REPRESENTATION_CONTEXT ( 'NONE', 'WORKASPACE' ) );
#1101=CIRCLE ( 'NONE', #800, 2.500000000000000888 ) ;
#1102=CARTESIAN_POINT ( 'NONE',  ( 2.500000000000000000, 2.357898499370432166, -2.385244779468109755E-15 ) ) ;
#1125=ADVANCED_FACE ( 'NONE', ( #8381 ), #5532, .F. ) ;
#1131=PLANE ( 'NONE',  #4489 ) ;
#1140=ORIENTED_EDGE ( 'NONE', *, *, #865, .F. ) ;
#1148=VECTOR ( 'NONE', #18172, 1000.000000000000000 ) ;
#1161=PLANE ( 'NONE',  #8704 ) ;
#1169=VECTOR ( 'NONE', #13558, 1000.000000000000114 ) ;
#1173=CIRCLE ( 'NONE', #2073, 2.041999999999999815 ) ;
#1242=DIRECTION ( 'NONE',  ( 0.000000000000000000, 0.000000000000000000, 1.000000000000000000 ) ) ;
#1249=CARTESIAN_POINT ( 'NONE',  ( 2.500000000000000000, -1.768423874527824902, -1.020999999999998353 ) ) ;
#1276=LINE ( 'NONE', #5644, #14756 ) ;
#1289=LINE ( 'NONE', #14331, #3976 ) ;
#1293=TOROIDAL_SURFACE ( 'NONE', #11005, 2.700000000000000622, 0.2000000000000000111 ) ;
#1303=FILL_AREA_STYLE_COLOUR ( '', #13221 ) ;
#1307=CARTESIAN_POINT ( 'NONE',  ( 2.500000000000000000, -1.178949249685218081, -2.041999999999998039 ) ) ;
#1393=CIRCLE ( 'NONE', #5656, 2.041999999999999815 ) ;
#1403=DIRECTION ( 'NONE',  ( 0.000000000000000000, 0.000000000000000000, 1.000000000000000000 ) ) ;
#1446=DIRECTION ( 'NONE',  ( -0.5000000000000051070, 0.000000000000000000, 0.8660254037844355990 ) ) ;
#1471=AXIS2_PLACEMENT_3D ( 'NONE', #4788, #17833, #10597 ) ;
#1498=ORIENTED_EDGE ( 'NONE', *, *, #3408, .T. ) ;
#1588=ADVANCED_FACE ( 'NONE', ( #3656 ), #14986, .T. ) ;
#1605=CARTESIAN_POINT ( 'NONE',  ( -31.74999999999995737, 3.061616997868383634E-16, -2.500000000000000444 ) ) ;
#1607=ORIENTED_EDGE ( 'NONE', *, *, #13546, .F. ) ;
#1609=EDGE_CURVE ( 'NONE', #15264, #2861, #7927, .T. ) ;
#1629=CARTESIAN_POINT ( 'NONE',  ( -31.74999999999995737, 0.000000000000000000, 4.250000000000000000 ) ) ;
#1670=DIRECTION ( 'NONE',  ( -0.000000000000000000, 0.000000000000000000, 1.000000000000000000 ) ) ;
#1679=ORIENTED_EDGE ( 'NONE', *, *, #9992, .T. ) ;
#1689=EDGE_LOOP ( 'NONE', ( #1498, #18620, #13343, #3428 ) ) ;
#1706=LINE ( 'NONE', #10461, #2400 ) ;
#1718=CARTESIAN_POINT ( 'NONE',  ( 2.500000000000000000, 1.178949249685213863, -2.042000000000001148 ) ) ;
#1733=ADVANCED_FACE ( 'NONE', ( #8318 ), #1760, .T. ) ;
#1760=TOROIDAL_SURFACE ( 'NONE', #16357, 4.000000000000000000, 0.2500000000000000000 ) ;
#1776=ORIENTED_EDGE ( 'NONE', *, *, #1609, .T. ) ;
#1813=AXIS2_PLACEMENT_3D ( 'NONE', #3741, #9640, #6314 ) ;
#1896=ADVANCED_FACE ( 'NONE', ( #11453 ), #16057, .T. ) ;
#1898=EDGE_CURVE ( 'NONE', #11226, #15342, #11829, .T. ) ;
#1907=PLANE ( 'NONE',  #17911 ) ;
#1931=CARTESIAN_POINT ( 'NONE',  ( -31.74999999999995737, 0.000000000000000000, 0.000000000000000000 ) ) ;
#1945=VERTEX_POINT ( 'NONE', #16115 ) ;
#1953=UNCERTAINTY_MEASURE_WITH_UNIT (LENGTH_MEASURE( 1.000000000000000082E-05 ), #4222, 'distance_accuracy_value', 'NONE');
#2001=EDGE_CURVE ( 'NONE', #9477, #13093, #2002, .T. ) ;
#2002=LINE ( 'NONE', #4864, #5114 ) ;
#2007=EDGE_CURVE ( 'NONE', #9233, #7319, #3303, .T. ) ;
#2021=DIRECTION ( 'NONE',  ( 0.000000000000000000, 0.000000000000000000, 1.000000000000000000 ) ) ;
#2022=CARTESIAN_POINT ( 'NONE',  ( 2.500000000000000000, 2.357898499370432166, -2.385244779468109755E-15 ) ) ;
#2071=ORIENTED_EDGE ( 'NONE', *, *, #2237, .F. ) ;
#2073=AXIS2_PLACEMENT_3D ( 'NONE', #6628, #12618, #2525 ) ;
#2091=DIRECTION ( 'NONE',  ( 0.000000000000000000, 0.000000000000000000, 1.000000000000000000 ) ) ;
#2095=DIRECTION ( 'NONE',  ( 0.000000000000000000, -0.5000000000000011102, -0.8660254037844379305 ) ) ;
#2134=DIRECTION ( 'NONE',  ( 0.000000000000000000, -0.8660254037844390407, -0.4999999999999992784 ) ) ;
#2164=DIRECTION ( 'NONE',  ( 0.000000000000000000, 0.000000000000000000, 1.000000000000000000 ) ) ;
#2187=ORIENTED_EDGE ( 'NONE', *, *, #16222, .F. ) ;
#2191=LINE ( 'NONE', #584, #12991 ) ;
#2194=DIRECTION ( 'NONE',  ( -1.000000000000000000, -0.000000000000000000, -0.000000000000000000 ) ) ;
#2209=PLANE ( 'NONE',  #7316 ) ;
#2237=EDGE_CURVE ( 'NONE', #15264, #16644, #9523, .T. ) ;
#2238=EDGE_CURVE ( 'NONE', #13691, #9705, #13915, .T. ) ;
#2259=CARTESIAN_POINT ( 'NONE',  ( 34.99999999999999289, 2.055000000000000160, 0.000000000000000000 ) ) ;
#2263=VERTEX_POINT ( 'NONE', #4293 ) ;
#2275=ORIENTED_EDGE ( 'NONE', *, *, #14138, .T. ) ;
#2282=CARTESIAN_POINT ( 'NONE',  ( 2.500000000000000000, 2.357898499370432166, -2.385244779468109755E-15 ) ) ;
#2283=CARTESIAN_POINT ( 'NONE',  ( 0.000000000000000000, -1.178949249685213863, 2.042000000000001148 ) ) ;
#2333=ORIENTED_EDGE ( 'NONE', *, *, #13301, .F. ) ;
#2374=EDGE_CURVE ( 'NONE', #4026, #9705, #10003, .T. ) ;
#2395=CARTESIAN_POINT ( 'NONE',  ( 2.500000000000000000, -1.178949249685213863, 2.042000000000001148 ) ) ;
#2400=VECTOR ( 'NONE', #17902, 1000.000000000000000 ) ;
#2472=DIRECTION ( 'NONE',  ( -1.000000000000000000, -0.000000000000000000, -0.000000000000000000 ) ) ;
#2479=CARTESIAN_POINT ( 'NONE',  ( 2.500000000000000000, -1.178949249685213863, 2.042000000000001148 ) ) ;
#2525=DIRECTION ( 'NONE',  ( 0.000000000000000000, 0.000000000000000000, 1.000000000000000000 ) ) ;
#2544=DIRECTION ( 'NONE',  ( 0.000000000000000000, 0.000000000000000000, -1.000000000000000000 ) ) ;
#2552=ORIENTED_EDGE ( 'NONE', *, *, #14420, .F. ) ;
#2572=( GEOMETRIC_REPRESENTATION_CONTEXT ( 3 ) GLOBAL_UNCERTAINTY_ASSIGNED_CONTEXT ( ( #1030 ) ) GLOBAL_UNIT_ASSIGNED_CONTEXT ( ( #12629, #11201, #17028 ) ) REPRESENTATION_CONTEXT ( 'NONE', 'WORKASPACE' ) );
#2601=FACE_OUTER_BOUND ( 'NONE', #13429, .T. ) ;
#2609=DIRECTION ( 'NONE',  ( 0.000000000000000000, -0.5000000000000011102, -0.8660254037844379305 ) ) ;
#2630=AXIS2_PLACEMENT_3D ( 'NONE', #8418, #2472, #15244 ) ;
#2675=DIRECTION ( 'NONE',  ( 0.000000000000000000, 0.8660254037844380415, -0.5000000000000009992 ) ) ;
#2687=ORIENTED_EDGE ( 'NONE', *, *, #2001, .T. ) ;
#2735=EDGE_CURVE ( 'NONE', #2861, #17956, #13669, .T. ) ;
#2759=EDGE_CURVE ( 'NONE', #125, #13093, #581, .T. ) ;
#2781=AXIS2_PLACEMENT_3D ( 'NONE', #823, #5190, #6345 ) ;
#2797=PRODUCT_CONTEXT ( 'NONE', #8284, 'mechanical' ) ;
#2805=DIRECTION ( 'NONE',  ( 1.000000000000000000, 0.000000000000000000, 0.000000000000000000 ) ) ;
#2861=VERTEX_POINT ( 'NONE', #10629 ) ;
#2873=LINE ( 'NONE', #14487, #337 ) ;
#2878=CARTESIAN_POINT ( 'NONE',  ( 2.500000000000000000, 1.178949249685213863, -2.042000000000001148 ) ) ;
#2918=ORIENTED_EDGE ( 'NONE', *, *, #18618, .T. ) ;
#2922=CARTESIAN_POINT ( 'NONE',  ( 34.55500000000001393, 0.000000000000000000, 0.000000000000000000 ) ) ;
#3015=ORIENTED_EDGE ( 'NONE', *, *, #2001, .F. ) ;
#3045=DIRECTION ( 'NONE',  ( -1.000000000000000000, -0.000000000000000000, -0.000000000000000000 ) ) ;
#3103=FILL_AREA_STYLE ('',( #1303 ) ) ;
#3112=PLANE ( 'NONE',  #15248 ) ;
#3211=ORIENTED_EDGE ( 'NONE', *, *, #11591, .T. ) ;
#3269=FACE_OUTER_BOUND ( 'NONE', #6748, .T. ) ;
#3279=ORIENTED_EDGE ( 'NONE', *, *, #11591, .F. ) ;
#3303=CIRCLE ( 'NONE', #14539, 4.250000000000000000 ) ;
#3313=ORIENTED_EDGE ( 'NONE', *, *, #9224, .T. ) ;
#3350=DIRECTION ( 'NONE',  ( 0.000000000000000000, -0.4999999999999992228, 0.8660254037844390407 ) ) ;
#3408=EDGE_CURVE ( 'NONE', #13093, #125, #1101, .T. ) ;
#3418=ORIENTED_EDGE ( 'NONE', *, *, #2007, .F. ) ;
#3423=FACE_OUTER_BOUND ( 'NONE', #3682, .T. ) ;
#3428=ORIENTED_EDGE ( 'NONE', *, *, #5058, .F. ) ;
#3497=DIRECTION ( 'NONE',  ( -0.000000000000000000, 0.8660254037844391517, 0.4999999999999991673 ) ) ;
#3520=CIRCLE ( 'NONE', #14157, 0.2000000000000000944 ) ;
#3533=DIRECTION ( 'NONE',  ( -0.7071067811865254793, 0.000000000000000000, 0.7071067811865695552 ) ) ;
#3587=CARTESIAN_POINT ( 'NONE',  ( 3.678949249685231848, 0.000000000000000000, 0.000000000000000000 ) ) ;
#3600=DIRECTION ( 'NONE',  ( 0.000000000000000000, -0.4999999999999991118, 0.8660254037844390407 ) ) ;
#3604=CARTESIAN_POINT ( 'NONE',  ( 5.200000000000002842, 0.000000000000000000, 0.000000000000000000 ) ) ;
#3608=EDGE_LOOP ( 'NONE', ( #1027, #5900, #1607 ) ) ;
#3616=LINE ( 'NONE', #10827, #9810 ) ;
#3641=PLANE ( 'NONE',  #12098 ) ;
#3656=FACE_OUTER_BOUND ( 'NONE', #1689, .T. ) ;
#3668=CARTESIAN_POINT ( 'NONE',  ( 34.99999999999999289, 0.000000000000000000, 0.000000000000000000 ) ) ;
#3682=EDGE_LOOP ( 'NONE', ( #2187, #18709, #11670, #10783 ) ) ;
#3698=ORIENTED_EDGE ( 'NONE', *, *, #12632, .F. ) ;
#3713=AXIS2_PLACEMENT_3D ( 'NONE', #3668, #18039, #7745 ) ;
#3741=CARTESIAN_POINT ( 'NONE',  ( 5.000000000000000888, 0.000000000000000000, 0.000000000000000000 ) ) ;
#3743=DIRECTION ( 'NONE',  ( 0.000000000000000000, 0.000000000000000000, 1.000000000000000000 ) ) ;
#3773=CARTESIAN_POINT ( 'NONE',  ( 5.200000000000002842, 0.000000000000000000, 0.000000000000000000 ) ) ;
#3801=STYLED_ITEM ( 'NONE', ( #16053 ), #13523 ) ;
#3884=LINE ( 'NONE', #13981, #4583 ) ;
#3890=VECTOR ( 'NONE', #7156, 1000.000000000000000 ) ;
#3920=CIRCLE ( 'NONE', #7247, 4.000000000000000000 ) ;
#3963=CARTESIAN_POINT ( 'NONE',  ( 34.99999999999999289, 0.000000000000000000, 2.055000000000000160 ) ) ;
#3976=VECTOR ( 'NONE', #9661, 1000.000000000000114 ) ;
#4016=ORIENTED_EDGE ( 'NONE', *, *, #10056, .T. ) ;
#4019=AXIS2_PLACEMENT_3D ( 'NONE', #8589, #5913, #10119 ) ;
#4026=VERTEX_POINT ( 'NONE', #17970 ) ;
#4123=EDGE_CURVE ( 'NONE', #13348, #11649, #6817, .T. ) ;
#4126=DIRECTION ( 'NONE',  ( 0.000000000000000000, 0.000000000000000000, -1.000000000000000000 ) ) ;
#4138=SHAPE_DEFINITION_REPRESENTATION ( #7701, #16765 ) ;
#4140=ORIENTED_EDGE ( 'NONE', *, *, #865, .T. ) ;
#4159=ORIENTED_EDGE ( 'NONE', *, *, #11695, .F. ) ;
#4222=( LENGTH_UNIT ( ) NAMED_UNIT ( * ) SI_UNIT ( .MILLI., .METRE. ) );
#4224=DIRECTION ( 'NONE',  ( -1.000000000000000000, -0.000000000000000000, -0.000000000000000000 ) ) ;
#4256=CARTESIAN_POINT ( 'NONE',  ( 2.500000000000000000, -1.178949249685213863, 2.042000000000001148 ) ) ;
#4274=ORIENTED_EDGE ( 'NONE', *, *, #8429, .T. ) ;
#4292=CARTESIAN_POINT ( 'NONE',  ( 2.500000000000000000, -1.178949249685213863, 2.042000000000001148 ) ) ;
#4293=CARTESIAN_POINT ( 'NONE',  ( 2.500000000000000000, -2.357898499370431722, 2.818925648462311528E-15 ) ) ;
#4342=ORIENTED_EDGE ( 'NONE', *, *, #12764, .T. ) ;
#4387=CARTESIAN_POINT ( 'NONE',  ( 0.2500000000000002220, 0.000000000000000000, 4.250000000000000000 ) ) ;
#4397=PLANE ( 'NONE',  #5224 ) ;
#4427=SURFACE_STYLE_USAGE ( .BOTH. , #17312 ) ;
#4434=VECTOR ( 'NONE', #2609, 1000.000000000000114 ) ;
#4441=ORIENTED_EDGE ( 'NONE', *, *, #18443, .F. ) ;
#4489=AXIS2_PLACEMENT_3D ( 'NONE', #2259, #8072, #2544 ) ;
#4497=AXIS2_PLACEMENT_3D ( 'NONE', #11576, #2805, #16137 ) ;
#4573=CIRCLE ( 'NONE', #14624, 2.041999999999999815 ) ;
#4583=VECTOR ( 'NONE', #3350, 1000.000000000000114 ) ;
#4595=ADVANCED_FACE ( 'NONE', ( #13947 ), #13670, .T. ) ;
#4602=DIRECTION ( 'NONE',  ( 0.000000000000000000, 0.000000000000000000, 1.000000000000000000 ) ) ;
#4692=ADVANCED_FACE ( 'NONE', ( #2601 ), #11454, .T. ) ;
#4694=LINE ( 'NONE', #11934, #14995 ) ;
#4748=ORIENTED_EDGE ( 'NONE', *, *, #4123, .F. ) ;
#4751=AXIS2_PLACEMENT_3D ( 'NONE', #7811, #13635, #12196 ) ;
#4784=DIRECTION ( 'NONE',  ( -1.000000000000000000, -0.000000000000000000, -0.000000000000000000 ) ) ;
#4788=CARTESIAN_POINT ( 'NONE',  ( 2.500000000000000000, 2.357898499370432166, -2.385244779468109755E-15 ) ) ;
#4864=CARTESIAN_POINT ( 'NONE',  ( 34.99999999999999289, 0.000000000000000000, 2.055000000000000160 ) ) ;
#4869=AXIS2_PLACEMENT_3D ( 'NONE', #5570, #8608, #6806 ) ;
#4897=VERTEX_POINT ( 'NONE', #1249 ) ;
#4903=ORIENTED_EDGE ( 'NONE', *, *, #12764, .F. ) ;
#4922=FACE_OUTER_BOUND ( 'NONE', #10487, .T. ) ;
#4966=FACE_OUTER_BOUND ( 'NONE', #4980, .T. ) ;
#4980=EDGE_LOOP ( 'NONE', ( #10664, #14620, #12544, #5870 ) ) ;
#4992=PLANE ( 'NONE',  #2781 ) ;
#4995=FACE_OUTER_BOUND ( 'NONE', #13965, .T. ) ;
#5032=ORIENTED_EDGE ( 'NONE', *, *, #9250, .F. ) ;
#5034=CONICAL_SURFACE ( 'NONE', #12344, 2.041999999999999815, 1.047197551196591858 ) ;
#5058=EDGE_CURVE ( 'NONE', #13093, #15064, #13609, .T. ) ;
#5079=ORIENTED_EDGE ( 'NONE', *, *, #16811, .T. ) ;
#5094=CIRCLE ( 'NONE', #5720, 4.250000000000000000 ) ;
#5098=CIRCLE ( 'NONE', #16972, 2.055000000000000160 ) ;
#5105=DIRECTION ( 'NONE',  ( 0.000000000000000000, 1.000000000000000000, -1.103561164596346103E-15 ) ) ;
#5114=VECTOR ( 'NONE', #3533, 1000.000000000000000 ) ;
#5150=DIRECTION ( 'NONE',  ( 0.000000000000000000, -1.000000000000000000, 1.103561164596346103E-15 ) ) ;
#5190=DIRECTION ( 'NONE',  ( 1.000000000000000000, 0.000000000000000000, 0.000000000000000000 ) ) ;
#5199=ORIENTED_EDGE ( 'NONE', *, *, #16704, .T. ) ;
#5213=ORIENTED_EDGE ( 'NONE', *, *, #2238, .F. ) ;
#5224=AXIS2_PLACEMENT_3D ( 'NONE', #17175, #7068, #4126 ) ;
#5377=VECTOR ( 'NONE', #16698, 1000.000000000000000 ) ;
#5513=DIRECTION ( 'NONE',  ( -1.000000000000000000, -0.000000000000000000, -0.000000000000000000 ) ) ;
#5528=ADVANCED_FACE ( 'NONE', ( #12460 ), #1131, .T. ) ;
#5532=PLANE ( 'NONE',  #17841 ) ;
#5570=CARTESIAN_POINT ( 'NONE',  ( 5.200000000000002842, 0.000000000000000000, -2.700000000000000622 ) ) ;
#5594=UNCERTAINTY_MEASURE_WITH_UNIT (LENGTH_MEASURE( 1.000000000000000082E-05 ), #8899, 'distance_accuracy_value', 'NONE');
#5605=ORIENTED_EDGE ( 'NONE', *, *, #9706, .F. ) ;
#5644=CARTESIAN_POINT ( 'NONE',  ( 0.000000000000000000, -1.178949249685213863, 2.042000000000001148 ) ) ;
#5656=AXIS2_PLACEMENT_3D ( 'NONE', #17124, #9869, #2164 ) ;
#5698=CARTESIAN_POINT ( 'NONE',  ( 2.500000000000000000, -2.629050547790028551E-15, -2.041999999999999815 ) ) ;
#5720=AXIS2_PLACEMENT_3D ( 'NONE', #7304, #5874, #11685 ) ;
#5745=FACE_OUTER_BOUND ( 'NONE', #12586, .T. ) ;
#5750=EDGE_CURVE ( 'NONE', #202, #858, #5094, .T. ) ;
#5791=ORIENTED_EDGE ( 'NONE', *, *, #15467, .F. ) ;
#5794=ORIENTED_EDGE ( 'NONE', *, *, #10503, .T. ) ;
#5813=PLANE ( 'NONE',  #6063 ) ;
#5828=CARTESIAN_POINT ( 'NONE',  ( 34.99999999999999289, 0.000000000000000000, 0.000000000000000000 ) ) ;
#5839=EDGE_LOOP ( 'NONE', ( #17998, #15562, #761, #1004, #5794 ) ) ;
#5851=CARTESIAN_POINT ( 'NONE',  ( 0.000000000000000000, 1.178949249685218081, 2.041999999999998483 ) ) ;
#5859=EDGE_LOOP ( 'NONE', ( #13206, #4441, #5605 ) ) ;
#5870=ORIENTED_EDGE ( 'NONE', *, *, #5750, .T. ) ;
#5871=FACE_BOUND ( 'NONE', #13970, .T. ) ;
#5874=DIRECTION ( 'NONE',  ( 1.000000000000000000, 0.000000000000000000, 0.000000000000000000 ) ) ;
#5900=ORIENTED_EDGE ( 'NONE', *, *, #17692, .F. ) ;
#5906=ADVANCED_FACE ( 'NONE', ( #4995 ), #15470, .F. ) ;
#5913=DIRECTION ( 'NONE',  ( 1.000000000000000000, 0.000000000000000000, 0.000000000000000000 ) ) ;
#5934=ORIENTED_EDGE ( 'NONE', *, *, #15467, .T. ) ;
#5947=CARTESIAN_POINT ( 'NONE',  ( 34.99999999999999289, 2.516649172247811061E-16, -2.055000000000000160 ) ) ;
#5954=EDGE_CURVE ( 'NONE', #15928, #13348, #1173, .T. ) ;
#5980=ORIENTED_EDGE ( 'NONE', *, *, #14420, .T. ) ;
#6063=AXIS2_PLACEMENT_3D ( 'NONE', #16187, #17, #9034 ) ;
#6082=DIRECTION ( 'NONE',  ( 0.000000000000000000, 1.000000000000000000, -1.103561164596346103E-15 ) ) ;
#6196=DIRECTION ( 'NONE',  ( -1.000000000000000000, -0.000000000000000000, -0.000000000000000000 ) ) ;
#6211=DIRECTION ( 'NONE',  ( -1.000000000000000000, -0.000000000000000000, -0.000000000000000000 ) ) ;
#6238=DIRECTION ( 'NONE',  ( -1.000000000000000000, 0.000000000000000000, -0.000000000000000000 ) ) ;
#6275=AXIS2_PLACEMENT_3D ( 'NONE', #7895, #13711, #2091 ) ;
#6314=DIRECTION ( 'NONE',  ( 0.000000000000000000, 0.000000000000000000, -1.000000000000000000 ) ) ;
#6345=DIRECTION ( 'NONE',  ( 0.000000000000000000, 0.000000000000000000, -1.000000000000000000 ) ) ;
#6380=LINE ( 'NONE', #15145, #7282 ) ;
#6388=DIRECTION ( 'NONE',  ( 0.000000000000000000, 0.5000000000000011102, 0.8660254037844380415 ) ) ;
#6406=DIRECTION ( 'NONE',  ( 1.000000000000000000, 0.000000000000000000, 0.000000000000000000 ) ) ;
#6415=ORIENTED_EDGE ( 'NONE', *, *, #12557, .T. ) ;
#6428=CARTESIAN_POINT ( 'NONE',  ( 2.500000000000000000, 2.500728763858895382E-16, -2.041999999999999815 ) ) ;
#6433=CIRCLE ( 'NONE', #3713, 2.055000000000000160 ) ;
#6448=PLANE ( 'NONE',  #13676 ) ;
#6495=CARTESIAN_POINT ( 'NONE',  ( 2.500000000000000000, 0.000000000000000000, 0.000000000000000000 ) ) ;
#6514=EDGE_LOOP ( 'NONE', ( #6415, #3313 ) ) ;
#6543=ORIENTED_EDGE ( 'NONE', *, *, #7593, .F. ) ;
#6584=AXIS2_PLACEMENT_3D ( 'NONE', #6612, #2134, #15362 ) ;
#6610=EDGE_LOOP ( 'NONE', ( #17338, #11011, #5934, #16175 ) ) ;
#6612=CARTESIAN_POINT ( 'NONE',  ( 2.500000000000000000, 2.357898499370432166, -2.385244779468109755E-15 ) ) ;
#6623=FACE_OUTER_BOUND ( 'NONE', #3608, .T. ) ;
#6628=CARTESIAN_POINT ( 'NONE',  ( 2.500000000000000000, 0.000000000000000000, 0.000000000000000000 ) ) ;
#6694=CARTESIAN_POINT ( 'NONE',  ( 2.500000000000000000, -1.178949249685213863, 2.042000000000001148 ) ) ;
#6748=EDGE_LOOP ( 'NONE', ( #7631, #10378, #950, #8623, #15637 ) ) ;
#6764=CARTESIAN_POINT ( 'NONE',  ( 2.500000000000000000, -1.178949249685218081, -2.041999999999998039 ) ) ;
#6771=CARTESIAN_POINT ( 'NONE',  ( 5.200000000000002842, 3.061616997868383634E-16, -2.500000000000000444 ) ) ;
#6773=ORIENTED_EDGE ( 'NONE', *, *, #2374, .T. ) ;
#6806=DIRECTION ( 'NONE',  ( 0.000000000000000000, 0.000000000000000000, -1.000000000000000000 ) ) ;
#6817=LINE ( 'NONE', #15583, #9912 ) ;
#6877=CARTESIAN_POINT ( 'NONE',  ( 0.000000000000000000, 5.051668046482832750E-16, -4.000000000000000000 ) ) ;
#6885=DIRECTION ( 'NONE',  ( 0.000000000000000000, -1.000000000000000000, 0.000000000000000000 ) ) ;
#6893=DIRECTION ( 'NONE',  ( -1.000000000000000000, -0.000000000000000000, -0.000000000000000000 ) ) ;
#6931=AXIS2_PLACEMENT_3D ( 'NONE', #410, #17932, #4602 ) ;
#6998=VECTOR ( 'NONE', #18033, 1000.000000000000000 ) ;
#7055=TOROIDAL_SURFACE ( 'NONE', #4019, 2.700000000000000622, 0.2000000000000000111 ) ;
#7068=DIRECTION ( 'NONE',  ( 1.000000000000000000, 0.000000000000000000, 0.000000000000000000 ) ) ;
#7073=ADVANCED_FACE ( 'NONE', ( #9135 ), #5813, .F. ) ;
#7094=ORIENTED_EDGE ( 'NONE', *, *, #16704, .F. ) ;
#7148=EDGE_CURVE ( 'NONE', #15064, #91, #17337, .T. ) ;
#7153=ORIENTED_EDGE ( 'NONE', *, *, #9395, .F. ) ;
#7156=DIRECTION ( 'NONE',  ( -1.000000000000000000, -0.000000000000000000, -0.000000000000000000 ) ) ;
#7157=FACE_OUTER_BOUND ( 'NONE', #11019, .T. ) ;
#7189=SHAPE_REPRESENTATION_RELATIONSHIP ( 'NONE' , 'NONE' ,  #16765, #13523 ) ;
#7247=AXIS2_PLACEMENT_3D ( 'NONE', #17622, #10289, #14576 ) ;
#7282=VECTOR ( 'NONE', #2095, 1000.000000000000114 ) ;
#7288=ORIENTED_EDGE ( 'NONE', *, *, #13615, .T. ) ;
#7304=CARTESIAN_POINT ( 'NONE',  ( 0.2500000000000002220, 0.000000000000000000, 0.000000000000000000 ) ) ;
#7316=AXIS2_PLACEMENT_3D ( 'NONE', #2022, #6406, #8014 ) ;
#7319=VERTEX_POINT ( 'NONE', #8708 ) ;
#7339=VERTEX_POINT ( 'NONE', #5851 ) ;
#7342=VECTOR ( 'NONE', #10473, 1000.000000000000000 ) ;
#7396=CARTESIAN_POINT ( 'NONE',  ( 0.2500000000000002220, 0.000000000000000000, 0.000000000000000000 ) ) ;
#7401=AXIS2_PLACEMENT_3D ( 'NONE', #910, #6885, #18512 ) ;
#7422=EDGE_CURVE ( 'NONE', #15264, #1945, #11584, .T. ) ;
#7467=( NAMED_UNIT ( * ) SI_UNIT ( $, .STERADIAN. ) SOLID_ANGLE_UNIT ( ) );
#7468=DIRECTION ( 'NONE',  ( 0.000000000000000000, 0.000000000000000000, -1.000000000000000000 ) ) ;
#7485=EDGE_CURVE ( 'NONE', #13348, #16644, #16054, .T. ) ;
#7568=ORIENTED_EDGE ( 'NONE', *, *, #7485, .T. ) ;
#7572=DIRECTION ( 'NONE',  ( 1.000000000000000000, 0.000000000000000000, 0.000000000000000000 ) ) ;
#7593=EDGE_CURVE ( 'NONE', #9087, #9477, #5098, .T. ) ;
#7623=FACE_OUTER_BOUND ( 'NONE', #13499, .T. ) ;
#7631=ORIENTED_EDGE ( 'NONE', *, *, #9992, .F. ) ;
#7664=CARTESIAN_POINT ( 'NONE',  ( 0.000000000000000000, 0.000000000000000000, 0.000000000000000000 ) ) ;
#7701=PRODUCT_DEFINITION_SHAPE ( 'NONE', 'NONE',  #13075 ) ;
#7708=CARTESIAN_POINT ( 'NONE',  ( 2.500000000000000000, -1.768423874527823125, 1.021000000000002128 ) ) ;
#7712=CARTESIAN_POINT ( 'NONE',  ( 2.500000000000000000, -1.178949249685213863, 2.042000000000001148 ) ) ;
#7731=DIRECTION ( 'NONE',  ( 0.000000000000000000, 0.000000000000000000, 1.000000000000000000 ) ) ;
#7740=ORIENTED_EDGE ( 'NONE', *, *, #18618, .F. ) ;
#7745=DIRECTION ( 'NONE',  ( 0.000000000000000000, 0.000000000000000000, 1.000000000000000000 ) ) ;
#7811=CARTESIAN_POINT ( 'NONE',  ( 0.2500000000000002220, 4.898587196589412829E-16, -4.000000000000000000 ) ) ;
#7831=AXIS2_PLACEMENT_3D ( 'NONE', #5828, #4224, #8864 ) ;
#7832=PLANE ( 'NONE',  #1471 ) ;
#7836=DIRECTION ( 'NONE',  ( -1.000000000000000000, -0.000000000000000000, -0.000000000000000000 ) ) ;
#7862=ORIENTED_EDGE ( 'NONE', *, *, #13301, .T. ) ;
#7894=DIRECTION ( 'NONE',  ( 0.000000000000000000, 0.4999999999999991118, -0.8660254037844391517 ) ) ;
#7895=CARTESIAN_POINT ( 'NONE',  ( -31.74999999999995737, 0.000000000000000000, 0.000000000000000000 ) ) ;
#7906=ORIENTED_EDGE ( 'NONE', *, *, #7593, .T. ) ;
#7927=LINE ( 'NONE', #9451, #1169 ) ;
#7982=CYLINDRICAL_SURFACE ( 'NONE', #6275, 2.500000000000000444 ) ;
#8014=DIRECTION ( 'NONE',  ( 0.000000000000000000, 0.000000000000000000, -1.000000000000000000 ) ) ;
#8017=AXIS2_PLACEMENT_3D ( 'NONE', #12801, #14324, #9934 ) ;
#8031=ADVANCED_FACE ( 'NONE', ( #9336 ), #3641, .F. ) ;
#8072=DIRECTION ( 'NONE',  ( 1.000000000000000000, 0.000000000000000000, 0.000000000000000000 ) ) ;
#8101=DIRECTION ( 'NONE',  ( 0.000000000000000000, -0.4999999999999992228, 0.8660254037844390407 ) ) ;
#8103=EDGE_LOOP ( 'NONE', ( #18176, #3418 ) ) ;
#8122=DIRECTION ( 'NONE',  ( -1.000000000000000000, -0.000000000000000000, -0.000000000000000000 ) ) ;
#8192=EDGE_CURVE ( 'NONE', #15342, #9705, #18770, .T. ) ;
#8284=APPLICATION_CONTEXT ( 'automotive_design' ) ;
#8309=AXIS2_PLACEMENT_3D ( 'NONE', #15645, #14220, #3743 ) ;
#8318=FACE_OUTER_BOUND ( 'NONE', #11196, .T. ) ;
#8334=EDGE_CURVE ( 'NONE', #17956, #13691, #1706, .T. ) ;
#8381=FACE_OUTER_BOUND ( 'NONE', #12103, .T. ) ;
#8418=CARTESIAN_POINT ( 'NONE',  ( 34.99999999999999289, 0.000000000000000000, 0.000000000000000000 ) ) ;
#8429=EDGE_CURVE ( 'NONE', #16875, #186, #3920, .T. ) ;
#8479=CARTESIAN_POINT ( 'NONE',  ( 2.500000000000000000, 1.178949249685213863, -2.042000000000001148 ) ) ;
#8495=CIRCLE ( 'NONE', #13367, 4.250000000000000000 ) ;
#8569=LINE ( 'NONE', #4292, #12373 ) ;
#8570=DIRECTION ( 'NONE',  ( 0.000000000000000000, 0.4999999999999991118, -0.8660254037844391517 ) ) ;
#8589=CARTESIAN_POINT ( 'NONE',  ( 5.200000000000002842, 0.000000000000000000, 0.000000000000000000 ) ) ;
#8595=PRODUCT ( 'socket head cap screw_iso_ISO 4762 M5 x 30 - 22N', 'socket head cap screw_iso_ISO 4762 M5 x 30 - 22N', '', ( #2797 ) ) ;
#8608=DIRECTION ( 'NONE',  ( 0.000000000000000000, -1.000000000000000000, 0.000000000000000000 ) ) ;
#8609=DIRECTION ( 'NONE',  ( 0.000000000000000000, 0.4999999999999991118, -0.8660254037844391517 ) ) ;
#8616=EDGE_CURVE ( 'NONE', #1945, #15342, #6380, .T. ) ;
#8618=DIRECTION ( 'NONE',  ( 0.000000000000000000, -0.5000000000000009992, -0.8660254037844380415 ) ) ;
#8623=ORIENTED_EDGE ( 'NONE', *, *, #9706, .T. ) ;
#8664=EDGE_CURVE ( 'NONE', #7319, #9233, #8495, .T. ) ;
#8704=AXIS2_PLACEMENT_3D ( 'NONE', #2479, #2675, #12576 ) ;
#8708=CARTESIAN_POINT ( 'NONE',  ( 5.000000000000004441, 0.000000000000000000, 4.250000000000000000 ) ) ;
#8864=DIRECTION ( 'NONE',  ( 0.000000000000000000, 0.000000000000000000, 1.000000000000000000 ) ) ;
#8899=( LENGTH_UNIT ( ) NAMED_UNIT ( * ) SI_UNIT ( .MILLI., .METRE. ) );
#8920=CIRCLE ( 'NONE', #7401, 0.2500000000000002220 ) ;
#9000=VERTEX_POINT ( 'NONE', #12167 ) ;
#9009=ADVANCED_FACE ( 'NONE', ( #4922 ), #6448, .T. ) ;
#9034=DIRECTION ( 'NONE',  ( 0.000000000000000000, 0.000000000000000000, -1.000000000000000000 ) ) ;
#9054=CARTESIAN_POINT ( 'NONE',  ( 5.000000000000000888, 0.000000000000000000, 0.000000000000000000 ) ) ;
#9063=EDGE_LOOP ( 'NONE', ( #12229, #14549, #11000, #17618, #9282 ) ) ;
#9068=ORIENTED_EDGE ( 'NONE', *, *, #2735, .F. ) ;
#9070=VECTOR ( 'NONE', #12483, 1000.000000000000000 ) ;
#9087=VERTEX_POINT ( 'NONE', #15496 ) ;
#9109=AXIS2_PLACEMENT_3D ( 'NONE', #3773, #9485, #9671 ) ;
#9118=DIRECTION ( 'NONE',  ( 1.000000000000000000, 0.000000000000000000, 0.000000000000000000 ) ) ;
#9135=FACE_OUTER_BOUND ( 'NONE', #260, .T. ) ;
#9224=EDGE_CURVE ( 'NONE', #9000, #14712, #10327, .T. ) ;
#9233=VERTEX_POINT ( 'NONE', #603 ) ;
#9250=EDGE_CURVE ( 'NONE', #10416, #17956, #12231, .T. ) ;
#9260=ORIENTED_EDGE ( 'NONE', *, *, #4123, .T. ) ;
#9273=VECTOR ( 'NONE', #10246, 1000.000000000000000 ) ;
#9280=DIRECTION ( 'NONE',  ( 0.000000000000000000, 1.224646799147353207E-16, 1.000000000000000000 ) ) ;
#9282=ORIENTED_EDGE ( 'NONE', *, *, #7422, .T. ) ;
#9325=PLANE ( 'NONE',  #16639 ) ;
#9336=FACE_OUTER_BOUND ( 'NONE', #15866, .T. ) ;
#9395=EDGE_CURVE ( 'NONE', #91, #14712, #10341, .T. ) ;
#9404=EDGE_CURVE ( 'NONE', #16644, #11649, #1289, .T. ) ;
#9425=ORIENTED_EDGE ( 'NONE', *, *, #8616, .F. ) ;
#9432=LINE ( 'NONE', #7712, #17212 ) ;
#9451=CARTESIAN_POINT ( 'NONE',  ( 2.500000000000000000, 2.357898499370432166, -2.385244779468109755E-15 ) ) ;
#9454=ORIENTED_EDGE ( 'NONE', *, *, #18443, .T. ) ;
#9477=VERTEX_POINT ( 'NONE', #3963 ) ;
#9485=DIRECTION ( 'NONE',  ( 1.000000000000000000, 0.000000000000000000, 0.000000000000000000 ) ) ;
#9523=LINE ( 'NONE', #2282, #12729 ) ;
#9561=DIRECTION ( 'NONE',  ( -1.000000000000000000, -0.000000000000000000, -0.000000000000000000 ) ) ;
#9590=ORIENTED_EDGE ( 'NONE', *, *, #12732, .F. ) ;
#9604=AXIS2_PLACEMENT_3D ( 'NONE', #9054, #6196, #11997 ) ;
#9611=ORIENTED_EDGE ( 'NONE', *, *, #9404, .F. ) ;
#9640=DIRECTION ( 'NONE',  ( -1.000000000000000000, -0.000000000000000000, -0.000000000000000000 ) ) ;
#9661=DIRECTION ( 'NONE',  ( 0.000000000000000000, -0.4999999999999992228, 0.8660254037844390407 ) ) ;
#9671=DIRECTION ( 'NONE',  ( 0.000000000000000000, 0.000000000000000000, -1.000000000000000000 ) ) ;
#9705=VERTEX_POINT ( 'NONE', #694 ) ;
#9706=EDGE_CURVE ( 'NONE', #4897, #15928, #4573, .T. ) ;
#9740=ADVANCED_FACE ( 'NONE', ( #16500 ), #2209, .F. ) ;
#9810=VECTOR ( 'NONE', #7894, 1000.000000000000000 ) ;
#9835=CARTESIAN_POINT ( 'NONE',  ( 0.2500000000000002220, 0.000000000000000000, 0.000000000000000000 ) ) ;
#9869=DIRECTION ( 'NONE',  ( -1.000000000000000000, -0.000000000000000000, -0.000000000000000000 ) ) ;
#9912=VECTOR ( 'NONE', #5105, 1000.000000000000000 ) ;
#9934=DIRECTION ( 'NONE',  ( 1.000000000000000000, 0.000000000000000000, 0.000000000000000000 ) ) ;
#9987=DIRECTION ( 'NONE',  ( -1.000000000000000000, -0.000000000000000000, -0.000000000000000000 ) ) ;
#9992=EDGE_CURVE ( 'NONE', #10416, #13348, #2873, .T. ) ;
#10003=LINE ( 'NONE', #15819, #15477 ) ;
#10056=EDGE_CURVE ( 'NONE', #1945, #7339, #3884, .T. ) ;
#10075=CARTESIAN_POINT ( 'NONE',  ( 2.500000000000000000, 0.000000000000000000, 0.000000000000000000 ) ) ;
#10110=ORIENTED_EDGE ( 'NONE', *, *, #12732, .T. ) ;
#10119=DIRECTION ( 'NONE',  ( 0.000000000000000000, 0.000000000000000000, -1.000000000000000000 ) ) ;
#10219=AXIS2_PLACEMENT_3D ( 'NONE', #13917, #2194, #18197 ) ;
#10239=SURFACE_STYLE_FILL_AREA ( #3103 ) ;
#10246=DIRECTION ( 'NONE',  ( -0.7071067811865254793, 8.659560562355202797E-17, -0.7071067811865695552 ) ) ;
#10289=DIRECTION ( 'NONE',  ( -1.000000000000000000, -0.000000000000000000, -0.000000000000000000 ) ) ;
#10291=CIRCLE ( 'NONE', #4497, 4.250000000000000000 ) ;
#10327=CIRCLE ( 'NONE', #1813, 2.700000000000000622 ) ;
#10334=CARTESIAN_POINT ( 'NONE',  ( 2.500000000000000000, 0.000000000000000000, 0.000000000000000000 ) ) ;
#10341=CIRCLE ( 'NONE', #4869, 0.2000000000000000944 ) ;
#10348=ORIENTED_EDGE ( 'NONE', *, *, #9224, .F. ) ;
#10351=ORIENTED_EDGE ( 'NONE', *, *, #16811, .F. ) ;
#10370=CARTESIAN_POINT ( 'NONE',  ( 2.500000000000000000, 1.178949249685218081, 2.041999999999998483 ) ) ;
#10378=ORIENTED_EDGE ( 'NONE', *, *, #9250, .T. ) ;
#10387=ADVANCED_FACE ( 'NONE', ( #5871, #16158 ), #3112, .T. ) ;
#10416=VERTEX_POINT ( 'NONE', #3587 ) ;
#10461=CARTESIAN_POINT ( 'NONE',  ( 2.500000000000000000, 1.178949249685213863, -2.042000000000001148 ) ) ;
#10469=( NAMED_UNIT ( * ) SI_UNIT ( $, .STERADIAN. ) SOLID_ANGLE_UNIT ( ) );
#10473=DIRECTION ( 'NONE',  ( -1.000000000000000000, -0.000000000000000000, -0.000000000000000000 ) ) ;
#10487=EDGE_LOOP ( 'NONE', ( #15753, #1140, #16745, #15516, #10501 ) ) ;
#10492=ADVANCED_FACE ( 'NONE', ( #536, #18330 ), #4992, .T. ) ;
#10501=ORIENTED_EDGE ( 'NONE', *, *, #2238, .T. ) ;
#10503=EDGE_CURVE ( 'NONE', #11649, #7339, #10799, .T. ) ;
#10597=DIRECTION ( 'NONE',  ( 0.000000000000000000, 0.000000000000000000, -1.000000000000000000 ) ) ;
#10611=EDGE_LOOP ( 'NONE', ( #2333, #7906, #2687, #16858 ) ) ;
#10629=CARTESIAN_POINT ( 'NONE',  ( 2.500000000000000000, 1.768423874527822903, -1.021000000000002350 ) ) ;
#10664=ORIENTED_EDGE ( 'NONE', *, *, #11405, .F. ) ;
#10667=DIRECTION ( 'NONE',  ( 0.000000000000000000, 0.000000000000000000, -1.000000000000000000 ) ) ;
#10688=DIRECTION ( 'NONE',  ( 0.000000000000000000, 1.000000000000000000, -1.103561164596346103E-15 ) ) ;
#10757=DIRECTION ( 'NONE',  ( -1.000000000000000000, -0.000000000000000000, -0.000000000000000000 ) ) ;
#10783=ORIENTED_EDGE ( 'NONE', *, *, #7148, .T. ) ;
#10799=LINE ( 'NONE', #16623, #18286 ) ;
#10827=CARTESIAN_POINT ( 'NONE',  ( 2.500000000000000000, -2.357898499370431722, 2.818925648462311528E-15 ) ) ;
#10847=CARTESIAN_POINT ( 'NONE',  ( 2.500000000000000000, 2.357898499370432166, -2.385244779468109755E-15 ) ) ;
#10858=ORIENTED_EDGE ( 'NONE', *, *, #7485, .F. ) ;
#10885=AXIS2_PLACEMENT_3D ( 'NONE', #14140, #9561, #17020 ) ;
#10946=DIRECTION ( 'NONE',  ( 0.000000000000000000, 0.8660254037844380415, -0.5000000000000011102 ) ) ;
#11000=ORIENTED_EDGE ( 'NONE', *, *, #14138, .F. ) ;
#11005=AXIS2_PLACEMENT_3D ( 'NONE', #14711, #7572, #7468 ) ;
#11011=ORIENTED_EDGE ( 'NONE', *, *, #11405, .T. ) ;
#11019=EDGE_LOOP ( 'NONE', ( #9260, #9611, #10858 ) ) ;
#11091=AXIS2_PLACEMENT_3D ( 'NONE', #3604, #9118, #14935 ) ;
#11196=EDGE_LOOP ( 'NONE', ( #4903, #613, #2918, #18591 ) ) ;
#11201=( NAMED_UNIT ( * ) PLANE_ANGLE_UNIT ( ) SI_UNIT ( $, .RADIAN. ) );
#11226=VERTEX_POINT ( 'NONE', #1718 ) ;
#11233=AXIS2_PLACEMENT_3D ( 'NONE', #2922, #5513, #17408 ) ;
#11312=DIRECTION ( 'NONE',  ( 0.000000000000000000, 0.000000000000000000, 1.000000000000000000 ) ) ;
#11341=CARTESIAN_POINT ( 'NONE',  ( 34.55500000000001393, 0.000000000000000000, 0.000000000000000000 ) ) ;
#11372=CARTESIAN_POINT ( 'NONE',  ( 2.500000000000000000, 2.357898499370432166, -2.385244779468109755E-15 ) ) ;
#11405=EDGE_CURVE ( 'NONE', #9233, #858, #2191, .T. ) ;
#11453=FACE_OUTER_BOUND ( 'NONE', #10611, .T. ) ;
#11454=CONICAL_SURFACE ( 'NONE', #2630, 2.055000000000000160, 0.7853981633974794763 ) ;
#11464=ORIENTED_EDGE ( 'NONE', *, *, #13615, .F. ) ;
#11517=EDGE_LOOP ( 'NONE', ( #16465, #4274 ) ) ;
#11538=( GEOMETRIC_REPRESENTATION_CONTEXT ( 3 ) GLOBAL_UNCERTAINTY_ASSIGNED_CONTEXT ( ( #1953 ) ) GLOBAL_UNIT_ASSIGNED_CONTEXT ( ( #4222, #13527, #10469 ) ) REPRESENTATION_CONTEXT ( 'NONE', 'WORKASPACE' ) );
#11576=CARTESIAN_POINT ( 'NONE',  ( 0.2500000000000002220, 0.000000000000000000, 0.000000000000000000 ) ) ;
#11584=LINE ( 'NONE', #14801, #6998 ) ;
#11591=EDGE_CURVE ( 'NONE', #14348, #13348, #8569, .T. ) ;
#11649=VERTEX_POINT ( 'NONE', #10370 ) ;
#11670=ORIENTED_EDGE ( 'NONE', *, *, #5058, .T. ) ;
#11685=DIRECTION ( 'NONE',  ( 0.000000000000000000, 0.000000000000000000, 1.000000000000000000 ) ) ;
#11695=EDGE_CURVE ( 'NONE', #14348, #12626, #15229, .T. ) ;
#11802=LINE ( 'NONE', #1605, #15347 ) ;
#11829=LINE ( 'NONE', #2878, #3890 ) ;
#11857=FACE_OUTER_BOUND ( 'NONE', #36, .T. ) ;
#11859=VECTOR ( 'NONE', #15203, 1000.000000000000114 ) ;
#11880=CARTESIAN_POINT ( 'NONE',  ( 2.500000000000000000, 2.253471898105738645E-15, 2.041999999999999815 ) ) ;
#11934=CARTESIAN_POINT ( 'NONE',  ( 0.000000000000000000, -1.178949249685213863, 2.042000000000001148 ) ) ;
#11973=DIRECTION ( 'NONE',  ( -1.000000000000000000, -0.000000000000000000, -0.000000000000000000 ) ) ;
#11997=DIRECTION ( 'NONE',  ( 0.000000000000000000, 0.000000000000000000, -1.000000000000000000 ) ) ;
#12081=CARTESIAN_POINT ( 'NONE',  ( 34.55500000000001393, 0.000000000000000000, 2.500000000000000888 ) ) ;
#12085=ORIENTED_EDGE ( 'NONE', *, *, #12277, .T. ) ;
#12098=AXIS2_PLACEMENT_3D ( 'NONE', #2395, #16973, #5150 ) ;
#12099=CARTESIAN_POINT ( 'NONE',  ( 5.000000000000004441, 0.000000000000000000, 0.000000000000000000 ) ) ;
#12103=EDGE_LOOP ( 'NONE', ( #17705, #5213, #15367, #2552, #18143 ) ) ;
#12167=CARTESIAN_POINT ( 'NONE',  ( 5.000000000000002665, 3.306546357697854226E-16, 2.700000000000000622 ) ) ;
#12196=DIRECTION ( 'NONE',  ( 0.000000000000000000, -1.224646799147353454E-16, 1.000000000000000000 ) ) ;
#12211=CYLINDRICAL_SURFACE ( 'NONE', #6931, 4.250000000000000000 ) ;
#12229=ORIENTED_EDGE ( 'NONE', *, *, #8616, .T. ) ;
#12231=LINE ( 'NONE', #6428, #11859 ) ;
#12277=EDGE_CURVE ( 'NONE', #12626, #4026, #1276, .T. ) ;
#12305=ORIENTED_EDGE ( 'NONE', *, *, #12277, .F. ) ;
#12344=AXIS2_PLACEMENT_3D ( 'NONE', #224, #4784, #2021 ) ;
#12373=VECTOR ( 'NONE', #6082, 1000.000000000000000 ) ;
#12460=FACE_OUTER_BOUND ( 'NONE', #785, .T. ) ;
#12483=DIRECTION ( 'NONE',  ( -1.000000000000000000, -0.000000000000000000, -0.000000000000000000 ) ) ;
#12544=ORIENTED_EDGE ( 'NONE', *, *, #17170, .T. ) ;
#12557=EDGE_CURVE ( 'NONE', #14712, #9000, #16000, .T. ) ;
#12576=DIRECTION ( 'NONE',  ( 0.000000000000000000, 0.5000000000000009992, 0.8660254037844380415 ) ) ;
#12586=EDGE_LOOP ( 'NONE', ( #11464, #16090, #12851, #10348 ) ) ;
#12604=CARTESIAN_POINT ( 'NONE',  ( 2.500000000000000000, -2.357898499370431722, 2.818925648462311528E-15 ) ) ;
#12618=DIRECTION ( 'NONE',  ( -1.000000000000000000, -0.000000000000000000, -0.000000000000000000 ) ) ;
#12626=VERTEX_POINT ( 'NONE', #2283 ) ;
#12629=( LENGTH_UNIT ( ) NAMED_UNIT ( * ) SI_UNIT ( .MILLI., .METRE. ) );
#12632=EDGE_CURVE ( 'NONE', #186, #16875, #15684, .T. ) ;
#12677=DIRECTION ( 'NONE',  ( 0.000000000000000000, 0.000000000000000000, 1.000000000000000000 ) ) ;
#12696=DIRECTION ( 'NONE',  ( 0.000000000000000000, 0.000000000000000000, 1.000000000000000000 ) ) ;
#12729=VECTOR ( 'NONE', #8101, 1000.000000000000114 ) ;
#12732=EDGE_CURVE ( 'NONE', #14348, #15928, #9432, .T. ) ;
#12764=EDGE_CURVE ( 'NONE', #858, #16875, #16291, .T. ) ;
#12801=CARTESIAN_POINT ( 'NONE',  ( 0.000000000000000000, 0.000000000000000000, 0.000000000000000000 ) ) ;
#12806=CARTESIAN_POINT ( 'NONE',  ( 0.2500000000000002220, 5.204748896376250699E-16, -4.250000000000000000 ) ) ;
#12836=ADVANCED_FACE ( 'NONE', ( #17251 ), #1161, .T. ) ;
#12851=ORIENTED_EDGE ( 'NONE', *, *, #9395, .T. ) ;
#12868=TOROIDAL_SURFACE ( 'NONE', #17713, 4.000000000000000000, 0.2500000000000000000 ) ;
#12884=ORIENTED_EDGE ( 'NONE', *, *, #5954, .F. ) ;
#12906=CARTESIAN_POINT ( 'NONE',  ( 2.500000000000000000, -2.357898499370431722, 2.818925648462311528E-15 ) ) ;
#12966=CARTESIAN_POINT ( 'NONE',  ( 34.55500000000001393, 3.061616997868384127E-16, -2.500000000000000888 ) ) ;
#12991=VECTOR ( 'NONE', #16571, 1000.000000000000000 ) ;
#13019=CARTESIAN_POINT ( 'NONE',  ( 5.200000000000002842, 3.306546357697854226E-16, 2.700000000000000622 ) ) ;
#13026=PRODUCT_DEFINITION_CONTEXT ( 'detailed design', #14371, 'design' ) ;
#13042=STYLED_ITEM('',(#18883),#15898);
#13051=DIRECTION ( 'NONE',  ( 0.000000000000000000, -1.287488025362403787E-15, -1.000000000000000000 ) ) ;
#13075=PRODUCT_DEFINITION ( 'UNKNOWN', '', #773, #13026 ) ;
#13092=ADVANCED_FACE ( 'NONE', ( #3423 ), #7982, .T. ) ;
#13093=VERTEX_POINT ( 'NONE', #12081 ) ;
#13206=ORIENTED_EDGE ( 'NONE', *, *, #15426, .F. ) ;
#13212=DIRECTION ( 'NONE',  ( -1.000000000000000000, -0.000000000000000000, -0.000000000000000000 ) ) ;
#13221=COLOUR_RGB ( '',1.000000000000000000, 0.9490196078431372140, 0.9098039215686274384 ) ;
#13225=CARTESIAN_POINT ( 'NONE',  ( -31.74999999999995737, 0.000000000000000000, 2.500000000000000444 ) ) ;
#13301=EDGE_CURVE ( 'NONE', #9087, #125, #17480, .T. ) ;
#13312=ORIENTED_EDGE ( 'NONE', *, *, #746, .F. ) ;
#13343=ORIENTED_EDGE ( 'NONE', *, *, #13416, .T. ) ;
#13348=VERTEX_POINT ( 'NONE', #11880 ) ;
#13357=DIRECTION ( 'NONE',  ( 0.000000000000000000, 0.000000000000000000, 1.000000000000000000 ) ) ;
#13367=AXIS2_PLACEMENT_3D ( 'NONE', #14287, #9987, #1242 ) ;
#13416=EDGE_CURVE ( 'NONE', #91, #15064, #18097, .T. ) ;
#13429=EDGE_LOOP ( 'NONE', ( #1040, #7862, #634, #3015 ) ) ;
#13443=CARTESIAN_POINT ( 'NONE',  ( 2.500000000000000000, 2.357898499370432166, -2.385244779468109755E-15 ) ) ;
#13499=EDGE_LOOP ( 'NONE', ( #2071, #1776, #10351 ) ) ;
#13523=ADVANCED_BREP_SHAPE_REPRESENTATION ( '', ( #15898, #8017 ), #2572 ) ;
#13527=( NAMED_UNIT ( * ) PLANE_ANGLE_UNIT ( ) SI_UNIT ( $, .RADIAN. ) );
#13531=MECHANICAL_DESIGN_GEOMETRIC_PRESENTATION_REPRESENTATION('',(#3801),#1069);
#13546=EDGE_CURVE ( 'NONE', #17956, #4897, #1393, .T. ) ;
#13558=DIRECTION ( 'NONE',  ( 0.000000000000000000, -0.5000000000000011102, -0.8660254037844379305 ) ) ;
#13609=LINE ( 'NONE', #13225, #17555 ) ;
#13615=EDGE_CURVE ( 'NONE', #15064, #9000, #3520, .T. ) ;
#13635=DIRECTION ( 'NONE',  ( -0.000000000000000000, 1.000000000000000000, 1.224646799147353207E-16 ) ) ;
#13652=FACE_OUTER_BOUND ( 'NONE', #16161, .T. ) ;
#13657=CARTESIAN_POINT ( 'NONE',  ( 2.500000000000000000, 1.768423874527825124, 1.020999999999998797 ) ) ;
#13669=CIRCLE ( 'NONE', #18531, 2.041999999999999815 ) ;
#13670=PLANE ( 'NONE',  #6584 ) ;
#13676=AXIS2_PLACEMENT_3D ( 'NONE', #16541, #3497, #3600 ) ;
#13691=VERTEX_POINT ( 'NONE', #1307 ) ;
#13711=DIRECTION ( 'NONE',  ( -1.000000000000000000, -0.000000000000000000, -0.000000000000000000 ) ) ;
#13822=LINE ( 'NONE', #18109, #5377 ) ;
#13915=LINE ( 'NONE', #6764, #9070 ) ;
#13917=CARTESIAN_POINT ( 'NONE',  ( 0.000000000000000000, 0.000000000000000000, 0.000000000000000000 ) ) ;
#13947=FACE_OUTER_BOUND ( 'NONE', #5839, .T. ) ;
#13965=EDGE_LOOP ( 'NONE', ( #5032, #1679, #7568, #5079, #250 ) ) ;
#13970=EDGE_LOOP ( 'NONE', ( #4016, #7094, #12085, #6773, #14843, #9425 ) ) ;
#13981=CARTESIAN_POINT ( 'NONE',  ( 0.000000000000000000, 2.357898499370432166, -2.385244779468109755E-15 ) ) ;
#14038=CARTESIAN_POINT ( 'NONE',  ( 34.99999999999999289, 0.000000000000000000, 0.000000000000000000 ) ) ;
#14049=PLANE ( 'NONE',  #847 ) ;
#14123=DIRECTION ( 'NONE',  ( -1.000000000000000000, -0.000000000000000000, -0.000000000000000000 ) ) ;
#14138=EDGE_CURVE ( 'NONE', #2861, #11226, #15662, .T. ) ;
#14140=CARTESIAN_POINT ( 'NONE',  ( 2.500000000000000000, 0.000000000000000000, 0.000000000000000000 ) ) ;
#14157=AXIS2_PLACEMENT_3D ( 'NONE', #13019, #16060, #9280 ) ;
#14220=DIRECTION ( 'NONE',  ( -1.000000000000000000, -0.000000000000000000, -0.000000000000000000 ) ) ;
#14234=ADVANCED_FACE ( 'NONE', ( #3269 ), #5034, .F. ) ;
#14287=CARTESIAN_POINT ( 'NONE',  ( 5.000000000000004441, 0.000000000000000000, 0.000000000000000000 ) ) ;
#14319=DIRECTION ( 'NONE',  ( 0.000000000000000000, -0.5000000000000009992, -0.8660254037844380415 ) ) ;
#14324=DIRECTION ( 'NONE',  ( 0.000000000000000000, 0.000000000000000000, 1.000000000000000000 ) ) ;
#14331=CARTESIAN_POINT ( 'NONE',  ( 2.500000000000000000, 2.357898499370432166, -2.385244779468109755E-15 ) ) ;
#14348=VERTEX_POINT ( 'NONE', #6694 ) ;
#14371=APPLICATION_CONTEXT ( 'automotive_design' ) ;
#14391=CARTESIAN_POINT ( 'NONE',  ( 0.000000000000000000, 1.178949249685213863, -2.042000000000001148 ) ) ;
#14420=EDGE_CURVE ( 'NONE', #11226, #17956, #13822, .T. ) ;
#14431=CARTESIAN_POINT ( 'NONE',  ( 5.200000000000002842, 0.000000000000000000, 2.500000000000000444 ) ) ;
#14462=DIRECTION ( 'NONE',  ( 0.000000000000000000, 1.000000000000000000, -1.287488025362403787E-15 ) ) ;
#14473=CARTESIAN_POINT ( 'NONE',  ( 0.000000000000000000, 0.000000000000000000, 4.000000000000000000 ) ) ;
#14487=CARTESIAN_POINT ( 'NONE',  ( 2.500000000000000000, 0.000000000000000000, 2.041999999999999815 ) ) ;
#14515=ORIENTED_EDGE ( 'NONE', *, *, #10503, .F. ) ;
#14539=AXIS2_PLACEMENT_3D ( 'NONE', #12099, #10757, #13357 ) ;
#14549=ORIENTED_EDGE ( 'NONE', *, *, #1898, .F. ) ;
#14576=DIRECTION ( 'NONE',  ( 0.000000000000000000, 0.000000000000000000, 1.000000000000000000 ) ) ;
#14620=ORIENTED_EDGE ( 'NONE', *, *, #2007, .T. ) ;
#14624=AXIS2_PLACEMENT_3D ( 'NONE', #6495, #6211, #15075 ) ;
#14675=DIRECTION ( 'NONE',  ( 0.000000000000000000, 0.000000000000000000, 1.000000000000000000 ) ) ;
#14711=CARTESIAN_POINT ( 'NONE',  ( 5.200000000000002842, 0.000000000000000000, 0.000000000000000000 ) ) ;
#14712=VERTEX_POINT ( 'NONE', #16011 ) ;
#14728=FACE_OUTER_BOUND ( 'NONE', #18484, .T. ) ;
#14756=VECTOR ( 'NONE', #14319, 1000.000000000000114 ) ;
#14801=CARTESIAN_POINT ( 'NONE',  ( 2.500000000000000000, 2.357898499370432166, -2.385244779468109755E-15 ) ) ;
#14843=ORIENTED_EDGE ( 'NONE', *, *, #8192, .F. ) ;
#14874=DIRECTION ( 'NONE',  ( -1.000000000000000000, -0.000000000000000000, -0.000000000000000000 ) ) ;
#14935=DIRECTION ( 'NONE',  ( 0.000000000000000000, 0.000000000000000000, -1.000000000000000000 ) ) ;
#14986=CYLINDRICAL_SURFACE ( 'NONE', #548, 2.500000000000000444 ) ;
#14995=VECTOR ( 'NONE', #10688, 1000.000000000000000 ) ;
#15064=VERTEX_POINT ( 'NONE', #14431 ) ;
#15075=DIRECTION ( 'NONE',  ( 0.000000000000000000, 0.000000000000000000, 1.000000000000000000 ) ) ;
#15145=CARTESIAN_POINT ( 'NONE',  ( 0.000000000000000000, 2.357898499370432166, -2.385244779468109755E-15 ) ) ;
#15203=DIRECTION ( 'NONE',  ( -0.5000000000000051070, 1.060575238724903217E-16, -0.8660254037844355990 ) ) ;
#15229=LINE ( 'NONE', #753, #1148 ) ;
#15240=ADVANCED_FACE ( 'NONE', ( #6623 ), #14049, .F. ) ;
#15244=DIRECTION ( 'NONE',  ( 0.000000000000000000, 0.000000000000000000, 1.000000000000000000 ) ) ;
#15248=AXIS2_PLACEMENT_3D ( 'NONE', #7664, #6238, #1670 ) ;
#15250=DIRECTION ( 'NONE',  ( 0.000000000000000000, -0.5000000000000009992, -0.8660254037844380415 ) ) ;
#15264=VERTEX_POINT ( 'NONE', #18420 ) ;
#15268=DIRECTION ( 'NONE',  ( 0.000000000000000000, 0.000000000000000000, 1.000000000000000000 ) ) ;
#15342=VERTEX_POINT ( 'NONE', #16904 ) ;
#15347=VECTOR ( 'NONE', #11973, 1000.000000000000000 ) ;
#15362=DIRECTION ( 'NONE',  ( 0.000000000000000000, 0.4999999999999992784, -0.8660254037844390407 ) ) ;
#15367=ORIENTED_EDGE ( 'NONE', *, *, #8334, .F. ) ;
#15426=EDGE_CURVE ( 'NONE', #2263, #4897, #17380, .T. ) ;
#15444=AXIS2_PLACEMENT_3D ( 'NONE', #10334, #16427, #17847 ) ;
#15467=EDGE_CURVE ( 'NONE', #858, #202, #10291, .T. ) ;
#15470=CONICAL_SURFACE ( 'NONE', #10885, 2.041999999999999815, 1.047197551196591858 ) ;
#15477=VECTOR ( 'NONE', #8570, 1000.000000000000000 ) ;
#15482=DIRECTION ( 'NONE',  ( 0.000000000000000000, 0.000000000000000000, -1.000000000000000000 ) ) ;
#15496=CARTESIAN_POINT ( 'NONE',  ( 34.99999999999999289, 2.789133085058097101E-16, -2.055000000000000160 ) ) ;
#15516=ORIENTED_EDGE ( 'NONE', *, *, #17692, .T. ) ;
#15546=ADVANCED_FACE ( 'NONE', ( #13652 ), #7832, .F. ) ;
#15562=ORIENTED_EDGE ( 'NONE', *, *, #7422, .F. ) ;
#15583=CARTESIAN_POINT ( 'NONE',  ( 2.500000000000000000, -1.178949249685213863, 2.042000000000001148 ) ) ;
#15607=ADVANCED_FACE ( 'NONE', ( #4966 ), #12211, .T. ) ;
#15637=ORIENTED_EDGE ( 'NONE', *, *, #5954, .T. ) ;
#15645=CARTESIAN_POINT ( 'NONE',  ( 2.500000000000000000, 0.000000000000000000, 0.000000000000000000 ) ) ;
#15662=LINE ( 'NONE', #11372, #4434 ) ;
#15684=CIRCLE ( 'NONE', #10219, 4.000000000000000000 ) ;
#15753=ORIENTED_EDGE ( 'NONE', *, *, #2374, .F. ) ;
#15819=CARTESIAN_POINT ( 'NONE',  ( 0.000000000000000000, -2.357898499370431722, 2.818925648462311528E-15 ) ) ;
#15866=EDGE_LOOP ( 'NONE', ( #5199, #14515, #4748, #3279, #17482 ) ) ;
#15869=( NAMED_UNIT ( * ) PLANE_ANGLE_UNIT ( ) SI_UNIT ( $, .RADIAN. ) );
#15898=MANIFOLD_SOLID_BREP ( 'Hex', #105 ) ;
#15916=ADVANCED_FACE ( 'NONE', ( #16397 ), #17270, .T. ) ;
#15928=VERTEX_POINT ( 'NONE', #7708 ) ;
#15931=VECTOR ( 'NONE', #8618, 1000.000000000000114 ) ;
#15957=ADVANCED_FACE ( 'NONE', ( #7623 ), #1907, .F. ) ;
#16000=CIRCLE ( 'NONE', #9604, 2.700000000000000622 ) ;
#16011=CARTESIAN_POINT ( 'NONE',  ( 5.000000000000002665, 0.000000000000000000, -2.700000000000000622 ) ) ;
#16053=PRESENTATION_STYLE_ASSIGNMENT (( #4427 ) ) ;
#16054=CIRCLE ( 'NONE', #15444, 2.041999999999999815 ) ;
#16057=CONICAL_SURFACE ( 'NONE', #7831, 2.055000000000000160, 0.7853981633974794763 ) ;
#16060=DIRECTION ( 'NONE',  ( 0.000000000000000000, 1.000000000000000000, -1.224646799147353207E-16 ) ) ;
#16090=ORIENTED_EDGE ( 'NONE', *, *, #13416, .F. ) ;
#16115=CARTESIAN_POINT ( 'NONE',  ( 0.000000000000000000, 2.357898499370432166, -2.385244779468109755E-15 ) ) ;
#16137=DIRECTION ( 'NONE',  ( 0.000000000000000000, 0.000000000000000000, 1.000000000000000000 ) ) ;
#16158=FACE_OUTER_BOUND ( 'NONE', #11517, .T. ) ;
#16161=EDGE_LOOP ( 'NONE', ( #9590, #3211, #12884 ) ) ;
#16175=ORIENTED_EDGE ( 'NONE', *, *, #17170, .F. ) ;
#16187=CARTESIAN_POINT ( 'NONE',  ( 2.500000000000000000, 2.357898499370432166, -2.385244779468109755E-15 ) ) ;
#16222=EDGE_CURVE ( 'NONE', #125, #91, #11802, .T. ) ;
#16291=CIRCLE ( 'NONE', #4751, 0.2500000000000002220 ) ;
#16357=AXIS2_PLACEMENT_3D ( 'NONE', #9835, #8122, #12696 ) ;
#16397=FACE_OUTER_BOUND ( 'NONE', #6610, .T. ) ;
#16427=DIRECTION ( 'NONE',  ( -1.000000000000000000, -0.000000000000000000, -0.000000000000000000 ) ) ;
#16465=ORIENTED_EDGE ( 'NONE', *, *, #12632, .T. ) ;
#16500=FACE_OUTER_BOUND ( 'NONE', #5859, .T. ) ;
#16530=DIRECTION ( 'NONE',  ( -1.000000000000000000, -0.000000000000000000, -0.000000000000000000 ) ) ;
#16541=CARTESIAN_POINT ( 'NONE',  ( 2.500000000000000000, -2.357898499370431722, 2.818925648462311528E-15 ) ) ;
#16571=DIRECTION ( 'NONE',  ( -1.000000000000000000, -0.000000000000000000, -0.000000000000000000 ) ) ;
#16623=CARTESIAN_POINT ( 'NONE',  ( 2.500000000000000000, 1.178949249685218081, 2.041999999999998483 ) ) ;
#16639=AXIS2_PLACEMENT_3D ( 'NONE', #10847, #10946, #6388 ) ;
#16644=VERTEX_POINT ( 'NONE', #13657 ) ;
#16648=VECTOR ( 'NONE', #6893, 1000.000000000000000 ) ;
#16695=AXIS2_PLACEMENT_3D ( 'NONE', #17914, #14874, #14675 ) ;
#16698=DIRECTION ( 'NONE',  ( 0.000000000000000000, -1.000000000000000000, 1.287488025362403787E-15 ) ) ;
#16704=EDGE_CURVE ( 'NONE', #12626, #7339, #4694, .T. ) ;
#16745=ORIENTED_EDGE ( 'NONE', *, *, #15426, .T. ) ;
#16765=SHAPE_REPRESENTATION ( 'socket head cap screw_iso_ISO 4762 M5 x 30 - 22N', ( #8017 ), #2572 ) ;
#16767=EDGE_LOOP ( 'NONE', ( #12305, #4159, #10110, #9454, #4140 ) ) ;
#16811=EDGE_CURVE ( 'NONE', #16644, #2861, #18032, .T. ) ;
#16858=ORIENTED_EDGE ( 'NONE', *, *, #2759, .F. ) ;
#16875=VERTEX_POINT ( 'NONE', #6877 ) ;
#16904=CARTESIAN_POINT ( 'NONE',  ( 0.000000000000000000, 1.178949249685213863, -2.042000000000001148 ) ) ;
#16972=AXIS2_PLACEMENT_3D ( 'NONE', #14038, #14123, #15268 ) ;
#16973=DIRECTION ( 'NONE',  ( -0.000000000000000000, 1.103561164596346103E-15, 1.000000000000000000 ) ) ;
#17020=DIRECTION ( 'NONE',  ( 0.000000000000000000, 0.000000000000000000, 1.000000000000000000 ) ) ;
#17028=( NAMED_UNIT ( * ) SI_UNIT ( $, .STERADIAN. ) SOLID_ANGLE_UNIT ( ) );
#17035=ADVANCED_FACE ( 'NONE', ( #5745 ), #7055, .F. ) ;
#17077=ADVANCED_FACE ( 'NONE', ( #7157 ), #4397, .F. ) ;
#17124=CARTESIAN_POINT ( 'NONE',  ( 2.500000000000000000, 0.000000000000000000, 0.000000000000000000 ) ) ;
#17170=EDGE_CURVE ( 'NONE', #7319, #202, #17723, .T. ) ;
#17175=CARTESIAN_POINT ( 'NONE',  ( 2.500000000000000000, 2.357898499370432166, -2.385244779468109755E-15 ) ) ;
#17212=VECTOR ( 'NONE', #15250, 1000.000000000000114 ) ;
#17251=FACE_OUTER_BOUND ( 'NONE', #16767, .T. ) ;
#17270=CYLINDRICAL_SURFACE ( 'NONE', #16695, 4.250000000000000000 ) ;
#17287=LINE ( 'NONE', #12604, #16648 ) ;
#17303=VECTOR ( 'NONE', #17352, 1000.000000000000000 ) ;
#17305=LINE ( 'NONE', #4256, #15931 ) ;
#17312=SURFACE_SIDE_STYLE ('',( #10239 ) ) ;
#17337=CIRCLE ( 'NONE', #9109, 2.500000000000000444 ) ;
#17338=ORIENTED_EDGE ( 'NONE', *, *, #8664, .T. ) ;
#17352=DIRECTION ( 'NONE',  ( 0.000000000000000000, -1.000000000000000000, 1.287488025362403787E-15 ) ) ;
#17380=LINE ( 'NONE', #12906, #17883 ) ;
#17408=DIRECTION ( 'NONE',  ( 0.000000000000000000, 0.000000000000000000, 1.000000000000000000 ) ) ;
#17480=LINE ( 'NONE', #5947, #9273 ) ;
#17482=ORIENTED_EDGE ( 'NONE', *, *, #11695, .T. ) ;
#17555=VECTOR ( 'NONE', #3045, 1000.000000000000000 ) ;
#17618=ORIENTED_EDGE ( 'NONE', *, *, #1609, .F. ) ;
#17622=CARTESIAN_POINT ( 'NONE',  ( 0.000000000000000000, 0.000000000000000000, 0.000000000000000000 ) ) ;
#17692=EDGE_CURVE ( 'NONE', #4897, #13691, #3616, .T. ) ;
#17705=ORIENTED_EDGE ( 'NONE', *, *, #8192, .T. ) ;
#17713=AXIS2_PLACEMENT_3D ( 'NONE', #7396, #13212, #1403 ) ;
#17717=DIRECTION ( 'NONE',  ( 1.000000000000000000, 0.000000000000000000, 0.000000000000000000 ) ) ;
#17723=LINE ( 'NONE', #1629, #7342 ) ;
#17833=DIRECTION ( 'NONE',  ( 1.000000000000000000, 0.000000000000000000, 0.000000000000000000 ) ) ;
#17841=AXIS2_PLACEMENT_3D ( 'NONE', #8479, #13051, #14462 ) ;
#17847=DIRECTION ( 'NONE',  ( 0.000000000000000000, 0.000000000000000000, 1.000000000000000000 ) ) ;
#17883=VECTOR ( 'NONE', #8609, 1000.000000000000000 ) ;
#17902=DIRECTION ( 'NONE',  ( 0.000000000000000000, -1.000000000000000000, 1.287488025362403787E-15 ) ) ;
#17904=MECHANICAL_DESIGN_GEOMETRIC_PRESENTATION_REPRESENTATION('',(#13042),#11538);
#17911=AXIS2_PLACEMENT_3D ( 'NONE', #13443, #17717, #10667 ) ;
#17914=CARTESIAN_POINT ( 'NONE',  ( -31.74999999999995737, 0.000000000000000000, 0.000000000000000000 ) ) ;
#17932=DIRECTION ( 'NONE',  ( -1.000000000000000000, -0.000000000000000000, -0.000000000000000000 ) ) ;
#17956=VERTEX_POINT ( 'NONE', #5698 ) ;
#17970=CARTESIAN_POINT ( 'NONE',  ( 0.000000000000000000, -2.357898499370431722, 2.818925648462311528E-15 ) ) ;
#17974=ADVANCED_FACE ( 'NONE', ( #14728 ), #12868, .T. ) ;
#17998=ORIENTED_EDGE ( 'NONE', *, *, #10056, .F. ) ;
#18032=CIRCLE ( 'NONE', #8309, 2.041999999999999815 ) ;
#18033=DIRECTION ( 'NONE',  ( -1.000000000000000000, -0.000000000000000000, -0.000000000000000000 ) ) ;
#18039=DIRECTION ( 'NONE',  ( -1.000000000000000000, -0.000000000000000000, -0.000000000000000000 ) ) ;
#18097=CIRCLE ( 'NONE', #11091, 2.500000000000000444 ) ;
#18109=CARTESIAN_POINT ( 'NONE',  ( 2.500000000000000000, 1.178949249685213863, -2.042000000000001148 ) ) ;
#18143=ORIENTED_EDGE ( 'NONE', *, *, #1898, .T. ) ;
#18172=DIRECTION ( 'NONE',  ( -1.000000000000000000, -0.000000000000000000, -0.000000000000000000 ) ) ;
#18176=ORIENTED_EDGE ( 'NONE', *, *, #8664, .F. ) ;
#18197=DIRECTION ( 'NONE',  ( 0.000000000000000000, 0.000000000000000000, 1.000000000000000000 ) ) ;
#18286=VECTOR ( 'NONE', #16530, 1000.000000000000000 ) ;
#18290=ORIENTED_EDGE ( 'NONE', *, *, #12557, .F. ) ;
#18330=FACE_OUTER_BOUND ( 'NONE', #8103, .T. ) ;
#18420=CARTESIAN_POINT ( 'NONE',  ( 2.500000000000000000, 2.357898499370432166, -2.385244779468109755E-15 ) ) ;
#18443=EDGE_CURVE ( 'NONE', #15928, #2263, #17305, .T. ) ;
#18484=EDGE_LOOP ( 'NONE', ( #5791, #4342, #3698, #7740 ) ) ;
#18486=DIRECTION ( 'NONE',  ( -1.000000000000000000, -0.000000000000000000, -0.000000000000000000 ) ) ;
#18512=DIRECTION ( 'NONE',  ( 0.000000000000000000, 0.000000000000000000, -1.000000000000000000 ) ) ;
#18531=AXIS2_PLACEMENT_3D ( 'NONE', #10075, #18644, #11312 ) ;
#18591=ORIENTED_EDGE ( 'NONE', *, *, #8429, .F. ) ;
#18618=EDGE_CURVE ( 'NONE', #202, #186, #8920, .T. ) ;
#18620=ORIENTED_EDGE ( 'NONE', *, *, #16222, .T. ) ;
#18644=DIRECTION ( 'NONE',  ( -1.000000000000000000, -0.000000000000000000, -0.000000000000000000 ) ) ;
#18709=ORIENTED_EDGE ( 'NONE', *, *, #2759, .T. ) ;
#18770=LINE ( 'NONE', #14391, #17303 ) ;
#18877=COLOUR_RGB('Black',0.12,0.14,0.17);
#18878=FILL_AREA_STYLE_COLOUR('',#18877);
#18879=FILL_AREA_STYLE('',(#18878));
#18880=SURFACE_STYLE_FILL_AREA(#18879);
#18881=SURFACE_SIDE_STYLE('',(#18880));
#18882=SURFACE_STYLE_USAGE(.BOTH.,#18881);
#18883=PRESENTATION_STYLE_ASSIGNMENT((#18882));
ENDSEC;
END-ISO-10303-21;
